ISO-10303-21;
HEADER;
FILE_DESCRIPTION (('STEP AP214'),
    '1' );
FILE_NAME ('Phillips Screw.step',
    '2026-10-06T13:23:30',
    ( '' ),
    ( '' ),
    'SwSTEP 2.0',
    'SolidWorks 2020',
    '' );
FILE_SCHEMA (( 'AUTOMOTIVE_DESIGN' ));
ENDSEC;

DATA;
#11=AXIS2_PLACEMENT_3D ( 'NONE', #8337, #8458, #15612 ) ;
#22=EDGE_CURVE ( 'NONE', #8505, #15326, #21385, .T. ) ;
#45=VECTOR ( 'NONE', #10247, 1000.000000000000000 ) ;
#83=CARTESIAN_POINT ( 'NONE',  ( 6.499999999879999102, -3.000000000000000000, -135.2552959529999725 ) ) ;
#90=EDGE_CURVE ( 'NONE', #4045, #3279, #299, .T. ) ;
#157=DIRECTION ( 'NONE',  ( 0.000000000000000000, 1.000000000000000000, 0.000000000000000000 ) ) ;
#254=EDGE_CURVE ( 'NONE', #1659, #23125, #22884, .T. ) ;
#277=EDGE_CURVE ( 'NONE', #1162, #21810, #7303, .T. ) ;
#297=ORIENTED_EDGE ( 'NONE', *, *, #254, .T. ) ;
#299=LINE ( 'NONE', #2335, #3484 ) ;
#314=ORIENTED_EDGE ( 'NONE', *, *, #22, .F. ) ;
#337=ORIENTED_EDGE ( 'NONE', *, *, #14672, .T. ) ;
#462=AXIS2_PLACEMENT_3D ( 'NONE', #6637, #9837, #21169 ) ;
#468=DIRECTION ( 'NONE',  ( -1.000000000000000000, 0.000000000000000000, 0.000000000000000000 ) ) ;
#657=ORIENTED_EDGE ( 'NONE', *, *, #277, .T. ) ;
#661=AXIS2_PLACEMENT_3D ( 'NONE', #17645, #15626, #22893 ) ;
#681=EDGE_LOOP ( 'NONE', ( #5696, #5785, #21336, #12694 ) ) ;
#713=SURFACE_SIDE_STYLE ('',( #19911 ) ) ;
#739=CYLINDRICAL_SURFACE ( 'NONE', #11687, 1.499999999999999334 ) ;
#742=VECTOR ( 'NONE', #894, 1000.000000000000000 ) ;
#780=FACE_OUTER_BOUND ( 'NONE', #15265, .T. ) ;
#810=EDGE_CURVE ( 'NONE', #5749, #6401, #18935, .T. ) ;
#841=ORIENTED_EDGE ( 'NONE', *, *, #2753, .F. ) ;
#884=ORIENTED_EDGE ( 'NONE', *, *, #17515, .F. ) ;
#894=DIRECTION ( 'NONE',  ( 1.000000000000000000, 0.000000000000000000, 0.000000000000000000 ) ) ;
#926=DIRECTION ( 'NONE',  ( 1.000000000000000000, 0.000000000000000000, 0.000000000000000000 ) ) ;
#942=CARTESIAN_POINT ( 'NONE',  ( 4.999999999879999990, -1.500000000000000000, -135.4552959529999896 ) ) ;
#943=FACE_OUTER_BOUND ( 'NONE', #18495, .T. ) ;
#957=ORIENTED_EDGE ( 'NONE', *, *, #4177, .T. ) ;
#994=AXIS2_PLACEMENT_3D ( 'NONE', #15653, #1375, #10392 ) ;
#1015=VERTEX_POINT ( 'NONE', #9697 ) ;
#1039=VECTOR ( 'NONE', #23463, 1000.000000000000000 ) ;
#1075=AXIS2_PLACEMENT_3D ( 'NONE', #18241, #14778, #157 ) ;
#1092=CARTESIAN_POINT ( 'NONE',  ( 4.499999999879999102, -4.000000000000000000, -132.3031539049999878 ) ) ;
#1113=VECTOR ( 'NONE', #12362, 1000.000000000000000 ) ;
#1159=DIRECTION ( 'NONE',  ( 0.4794255386042040601, 0.8775825618903723147, 0.000000000000000000 ) ) ;
#1161=DIRECTION ( 'NONE',  ( 1.000000000000000000, 0.000000000000000000, 0.000000000000000000 ) ) ;
#1162=VERTEX_POINT ( 'NONE', #16258 ) ;
#1191=ORIENTED_EDGE ( 'NONE', *, *, #8125, .F. ) ;
#1256=CARTESIAN_POINT ( 'NONE',  ( 4.499999999879999102, -3.500000000000000000, -143.0552959529999839 ) ) ;
#1260=ORIENTED_EDGE ( 'NONE', *, *, #90, .T. ) ;
#1367=VECTOR ( 'NONE', #19078, 1000.000000000000000 ) ;
#1375=DIRECTION ( 'NONE',  ( 0.000000000000000000, 0.000000000000000000, -1.000000000000000000 ) ) ;
#1406=EDGE_CURVE ( 'NONE', #3396, #4045, #8593, .T. ) ;
#1447=DIRECTION ( 'NONE',  ( 1.000000000000000000, 0.000000000000000000, 0.000000000000000000 ) ) ;
#1506=VECTOR ( 'NONE', #4741, 1000.000000000000000 ) ;
#1569=ORIENTED_EDGE ( 'NONE', *, *, #5864, .T. ) ;
#1578=CARTESIAN_POINT ( 'NONE',  ( 4.499999999879999102, -1.500000000000000000, -135.0552959530000123 ) ) ;
#1594=CARTESIAN_POINT ( 'NONE',  ( 3.999999999879999546, -1.500000000000000000, -135.4552959529999896 ) ) ;
#1612=ORIENTED_EDGE ( 'NONE', *, *, #20797, .T. ) ;
#1659=VERTEX_POINT ( 'NONE', #21314 ) ;
#1713=ADVANCED_FACE ( 'NONE', ( #9986 ), #15826, .T. ) ;
#1834=EDGE_CURVE ( 'NONE', #11473, #21810, #8790, .T. ) ;
#1845=ADVANCED_FACE ( 'NONE', ( #19881 ), #12932, .T. ) ;
#1855=CARTESIAN_POINT ( 'NONE',  ( 3.999999999879999546, -4.750000000000000000, -135.4552959529999896 ) ) ;
#1858=ORIENTED_EDGE ( 'NONE', *, *, #21584, .T. ) ;
#1869=DIRECTION ( 'NONE',  ( 0.000000000000000000, 0.000000000000000000, 1.000000000000000000 ) ) ;
#1927=VECTOR ( 'NONE', #7417, 1000.000000000000000 ) ;
#1928=CARTESIAN_POINT ( 'NONE',  ( 6.499999999879999102, -3.500000000000000000, -143.0552959529999839 ) ) ;
#1940=EDGE_CURVE ( 'NONE', #15326, #12329, #5483, .T. ) ;
#1945=EDGE_LOOP ( 'NONE', ( #12442, #20011, #19749, #3060, #2593, #7811, #4743, #18994, #314, #1569, #11789, #3631 ) ) ;
#2036=ORIENTED_EDGE ( 'NONE', *, *, #4437, .F. ) ;
#2075=CARTESIAN_POINT ( 'NONE',  ( 3.999999999879999546, -3.000000000000000000, -135.2552959529999725 ) ) ;
#2088=FACE_OUTER_BOUND ( 'NONE', #14523, .T. ) ;
#2190=DIRECTION ( 'NONE',  ( 0.3989061605089001539, 0.7301928289268172501, 0.5547001962248612195 ) ) ;
#2199=FACE_OUTER_BOUND ( 'NONE', #7681, .T. ) ;
#2322=LINE ( 'NONE', #5982, #8614 ) ;
#2329=LINE ( 'NONE', #9424, #742 ) ;
#2335=CARTESIAN_POINT ( 'NONE',  ( 2.499999999879999990, -3.500000000000000000, -135.4552959529999896 ) ) ;
#2338=CARTESIAN_POINT ( 'NONE',  ( 4.999999999879999990, -3.500000000000000000, -132.9059375850000038 ) ) ;
#2480=EDGE_LOOP ( 'NONE', ( #6252, #957, #9033, #21625 ) ) ;
#2593=ORIENTED_EDGE ( 'NONE', *, *, #20659, .T. ) ;
#2617=ADVANCED_FACE ( 'NONE', ( #780 ), #11571, .T. ) ;
#2705=VECTOR ( 'NONE', #14475, 1000.000000000000000 ) ;
#2727=ORIENTED_EDGE ( 'NONE', *, *, #18960, .F. ) ;
#2746=EDGE_LOOP ( 'NONE', ( #14652, #1260, #8463, #21117 ) ) ;
#2753=EDGE_CURVE ( 'NONE', #16256, #6145, #3615, .T. ) ;
#2772=PLANE ( 'NONE',  #11 ) ;
#2808=DIRECTION ( 'NONE',  ( 0.000000000000000000, 0.000000000000000000, 1.000000000000000000 ) ) ;
#2833=CARTESIAN_POINT ( 'NONE',  ( 3.999999999879999546, -5.500000000000000000, -135.4552959529999896 ) ) ;
#2867=CARTESIAN_POINT ( 'NONE',  ( 4.999999999879999990, -3.500000000000000000, -132.9059375850000038 ) ) ;
#2911=ORIENTED_EDGE ( 'NONE', *, *, #4437, .T. ) ;
#2926=CARTESIAN_POINT ( 'NONE',  ( 4.499999999879999102, -3.500000000000000000, -136.0552959530000123 ) ) ;
#3014=CARTESIAN_POINT ( 'NONE',  ( 5.749999999879999102, -3.000000000000000000, -135.0552959530000123 ) ) ;
#3045=AXIS2_PLACEMENT_3D ( 'NONE', #3653, #21396, #10418 ) ;
#3060=ORIENTED_EDGE ( 'NONE', *, *, #6740, .F. ) ;
#3218=PRESENTATION_STYLE_ASSIGNMENT (( #12246 ) ) ;
#3279=VERTEX_POINT ( 'NONE', #21915 ) ;
#3366=( NAMED_UNIT ( * ) SI_UNIT ( $, .STERADIAN. ) SOLID_ANGLE_UNIT ( ) );
#3396=VERTEX_POINT ( 'NONE', #7270 ) ;
#3484=VECTOR ( 'NONE', #7542, 1000.000000000000000 ) ;
#3573=FILL_AREA_STYLE_COLOUR ( '', #22718 ) ;
#3598=ORIENTED_EDGE ( 'NONE', *, *, #277, .F. ) ;
#3609=FILL_AREA_STYLE_COLOUR ( '', #16458 ) ;
#3615=LINE ( 'NONE', #2075, #16874 ) ;
#3631=ORIENTED_EDGE ( 'NONE', *, *, #14672, .F. ) ;
#3639=CARTESIAN_POINT ( 'NONE',  ( 4.999999999879999990, -2.250000000000000000, -135.0552959530000123 ) ) ;
#3653=CARTESIAN_POINT ( 'NONE',  ( 4.499999999879999102, -3.500000000000000000, -136.0552959530000123 ) ) ;
#3709=EDGE_CURVE ( 'NONE', #1015, #22590, #5100, .T. ) ;
#3732=CARTESIAN_POINT ( 'NONE',  ( 3.780861691979999772, -4.816373842840000030, -136.0552959530000123 ) ) ;
#3771=ORIENTED_EDGE ( 'NONE', *, *, #21036, .F. ) ;
#3786=VECTOR ( 'NONE', #19370, 1000.000000000000000 ) ;
#3790=CARTESIAN_POINT ( 'NONE',  ( 6.499999999879999102, -3.500000000000000000, -135.4552959529999896 ) ) ;
#3845=ADVANCED_BREP_SHAPE_REPRESENTATION ( '', ( #19750, #5025 ), #9222 ) ;
#3916=VERTEX_POINT ( 'NONE', #21991 ) ;
#3943=PRODUCT_DEFINITION_FORMATION_WITH_SPECIFIED_SOURCE ( 'ANY', '', #5209, .NOT_KNOWN. ) ;
#4045=VERTEX_POINT ( 'NONE', #22811 ) ;
#4087=AXIS2_PLACEMENT_3D ( 'NONE', #2867, #15597, #19406 ) ;
#4093=VERTEX_POINT ( 'NONE', #17446 ) ;
#4095=ORIENTED_EDGE ( 'NONE', *, *, #21142, .T. ) ;
#4110=ORIENTED_EDGE ( 'NONE', *, *, #6634, .T. ) ;
#4177=EDGE_CURVE ( 'NONE', #15326, #8394, #19709, .T. ) ;
#4235=CARTESIAN_POINT ( 'NONE',  ( 4.999999999879999990, -1.500000000000000000, -135.0552959530000123 ) ) ;
#4267=VERTEX_POINT ( 'NONE', #4546 ) ;
#4281=ORIENTED_EDGE ( 'NONE', *, *, #8768, .F. ) ;
#4296=STYLED_ITEM ( 'NONE', ( #10840 ), #3845 ) ;
#4340=PLANE ( 'NONE',  #11011 ) ;
#4344=AXIS2_PLACEMENT_3D ( 'NONE', #8006, #15290, #6820 ) ;
#4416=DIRECTION ( 'NONE',  ( 1.000000000000000000, 0.000000000000000000, 0.000000000000000000 ) ) ;
#4437=EDGE_CURVE ( 'NONE', #8394, #21412, #12029, .T. ) ;
#4442=VECTOR ( 'NONE', #19186, 1000.000000000000000 ) ;
#4542=ORIENTED_EDGE ( 'NONE', *, *, #18951, .T. ) ;
#4546=CARTESIAN_POINT ( 'NONE',  ( 3.999999999879999546, -5.500000000000000000, -135.0552959530000123 ) ) ;
#4588=FACE_OUTER_BOUND ( 'NONE', #22076, .T. ) ;
#4590=CARTESIAN_POINT ( 'NONE',  ( 0.000000000000000000, 0.000000000000000000, 0.000000000000000000 ) ) ;
#4670=( GEOMETRIC_REPRESENTATION_CONTEXT ( 3 ) GLOBAL_UNCERTAINTY_ASSIGNED_CONTEXT ( ( #22799 ) ) GLOBAL_UNIT_ASSIGNED_CONTEXT ( ( #18007, #14559, #10726 ) ) REPRESENTATION_CONTEXT ( 'NONE', 'WORKASPACE' ) );
#4680=LINE ( 'NONE', #15278, #7575 ) ;
#4728=DIRECTION ( 'NONE',  ( 0.000000000000000000, 0.000000000000000000, 1.000000000000000000 ) ) ;
#4741=DIRECTION ( 'NONE',  ( 0.000000000000000000, 0.000000000000000000, -1.000000000000000000 ) ) ;
#4743=ORIENTED_EDGE ( 'NONE', *, *, #20662, .T. ) ;
#4765=CARTESIAN_POINT ( 'NONE',  ( 4.999999999879999990, -4.750000000000000000, -135.4552959529999896 ) ) ;
#4832=LINE ( 'NONE', #10293, #18689 ) ;
#4876=ADVANCED_FACE ( 'NONE', ( #6538 ), #17485, .T. ) ;
#5025=AXIS2_PLACEMENT_3D ( 'NONE', #4590, #17084, #1161 ) ;
#5056=DIRECTION ( 'NONE',  ( 0.000000000000000000, 0.000000000000000000, 1.000000000000000000 ) ) ;
#5089=CARTESIAN_POINT ( 'NONE',  ( 4.999999999879999990, -3.000000000000000000, -135.0552959530000123 ) ) ;
#5100=LINE ( 'NONE', #14264, #12152 ) ;
#5113=SURFACE_SIDE_STYLE ('',( #8904 ) ) ;
#5118=LINE ( 'NONE', #23212, #1113 ) ;
#5168=VECTOR ( 'NONE', #2190, 1000.000000000000000 ) ;
#5209=PRODUCT ( 'Phillips Screw', 'Phillips Screw', '', ( #18304 ) ) ;
#5228=LINE ( 'NONE', #14633, #7813 ) ;
#5239=( GEOMETRIC_REPRESENTATION_CONTEXT ( 3 ) GLOBAL_UNCERTAINTY_ASSIGNED_CONTEXT ( ( #23498 ) ) GLOBAL_UNIT_ASSIGNED_CONTEXT ( ( #19987, #10800, #18085 ) ) REPRESENTATION_CONTEXT ( 'NONE', 'WORKASPACE' ) );
#5363=LINE ( 'NONE', #14529, #12484 ) ;
#5418=ORIENTED_EDGE ( 'NONE', *, *, #6634, .F. ) ;
#5483=LINE ( 'NONE', #1578, #20173 ) ;
#5488=EDGE_CURVE ( 'NONE', #3279, #17827, #23139, .T. ) ;
#5589=DIRECTION ( 'NONE',  ( 0.000000000000000000, 1.000000000000000000, 0.000000000000000000 ) ) ;
#5650=DIRECTION ( 'NONE',  ( 0.000000000000000000, 0.000000000000000000, 1.000000000000000000 ) ) ;
#5672=ORIENTED_EDGE ( 'NONE', *, *, #5488, .F. ) ;
#5673=DIRECTION ( 'NONE',  ( 1.000000000000000000, 0.000000000000000000, 0.000000000000000000 ) ) ;
#5696=ORIENTED_EDGE ( 'NONE', *, *, #17515, .T. ) ;
#5749=VERTEX_POINT ( 'NONE', #15272 ) ;
#5785=ORIENTED_EDGE ( 'NONE', *, *, #12393, .F. ) ;
#5787=ORIENTED_EDGE ( 'NONE', *, *, #9768, .F. ) ;
#5821=EDGE_LOOP ( 'NONE', ( #2727, #13598, #7084, #6987 ) ) ;
#5858=CARTESIAN_POINT ( 'NONE',  ( 5.578707461739999651, -1.525439235750000178, -135.5552959530000123 ) ) ;
#5864=EDGE_CURVE ( 'NONE', #8505, #21499, #14069, .T. ) ;
#5942=ORIENTED_EDGE ( 'NONE', *, *, #21036, .T. ) ;
#5982=CARTESIAN_POINT ( 'NONE',  ( 3.999999999879999546, -1.500000000000000000, -135.2552959529999725 ) ) ;
#6020=DIRECTION ( 'NONE',  ( 0.000000000000000000, 0.000000000000000000, 1.000000000000000000 ) ) ;
#6041=EDGE_CURVE ( 'NONE', #13199, #21050, #20924, .T. ) ;
#6044=EDGE_CURVE ( 'NONE', #20527, #22590, #8281, .T. ) ;
#6063=VECTOR ( 'NONE', #1869, 1000.000000000000000 ) ;
#6145=VERTEX_POINT ( 'NONE', #9827 ) ;
#6225=DIRECTION ( 'NONE',  ( 0.000000000000000000, -1.000000000000000000, 0.000000000000000000 ) ) ;
#6252=ORIENTED_EDGE ( 'NONE', *, *, #22, .T. ) ;
#6255=EDGE_CURVE ( 'NONE', #3916, #11473, #13277, .T. ) ;
#6283=LINE ( 'NONE', #15338, #1506 ) ;
#6372=ORIENTED_EDGE ( 'NONE', *, *, #10361, .T. ) ;
#6401=VERTEX_POINT ( 'NONE', #16958 ) ;
#6406=AXIS2_PLACEMENT_3D ( 'NONE', #1928, #1447, #5589 ) ;
#6420=VECTOR ( 'NONE', #21335, 1000.000000000000000 ) ;
#6448=EDGE_LOOP ( 'NONE', ( #5942, #1858, #13046, #337 ) ) ;
#6538=FACE_OUTER_BOUND ( 'NONE', #17624, .T. ) ;
#6606=ORIENTED_EDGE ( 'NONE', *, *, #18951, .F. ) ;
#6634=EDGE_CURVE ( 'NONE', #21412, #12329, #2322, .T. ) ;
#6637=CARTESIAN_POINT ( 'NONE',  ( 3.999999999879999546, -3.500000000000000000, -135.4552959529999896 ) ) ;
#6727=ORIENTED_EDGE ( 'NONE', *, *, #90, .F. ) ;
#6740=EDGE_CURVE ( 'NONE', #3396, #21050, #22761, .T. ) ;
#6776=PLANE ( 'NONE',  #4087 ) ;
#6820=DIRECTION ( 'NONE',  ( 0.000000000000000000, 1.000000000000000000, 0.000000000000000000 ) ) ;
#6887=CLOSED_SHELL ( 'NONE', ( #23245, #16871, #1713, #13548, #19346, #10841, #20769, #19401, #7857, #2617, #10509, #19594, #9099, #19097, #15877, #1845, #20291, #4876, #7964 ) ) ;
#6902=PLANE ( 'NONE',  #6406 ) ;
#6908=EDGE_CURVE ( 'NONE', #20527, #4267, #16211, .T. ) ;
#6959=EDGE_LOOP ( 'NONE', ( #14711, #20420, #16785, #12576 ) ) ;
#6987=ORIENTED_EDGE ( 'NONE', *, *, #18400, .F. ) ;
#7012=CARTESIAN_POINT ( 'NONE',  ( 3.061723384069999998, -6.132747685670000060, -135.0552959530000123 ) ) ;
#7013=VERTEX_POINT ( 'NONE', #10476 ) ;
#7017=CARTESIAN_POINT ( 'NONE',  ( 4.499999999879999102, -3.500000000000000000, -136.0552959530000123 ) ) ;
#7051=APPLICATION_CONTEXT ( 'automotive_design' ) ;
#7084=ORIENTED_EDGE ( 'NONE', *, *, #15487, .T. ) ;
#7270=CARTESIAN_POINT ( 'NONE',  ( 2.499999999879999990, -4.000000000000000000, -135.0552959530000123 ) ) ;
#7303=CIRCLE ( 'NONE', #10698, 3.000000000000000000 ) ;
#7367=DIRECTION ( 'NONE',  ( 1.000000000000000000, 0.000000000000000000, 0.000000000000000000 ) ) ;
#7417=DIRECTION ( 'NONE',  ( 0.000000000000000000, 0.000000000000000000, 1.000000000000000000 ) ) ;
#7454=CARTESIAN_POINT ( 'NONE',  ( 4.499999999879999102, -1.500000000000000000, -143.0552959529999839 ) ) ;
#7466=ORIENTED_EDGE ( 'NONE', *, *, #810, .T. ) ;
#7482=CARTESIAN_POINT ( 'NONE',  ( 5.219138307789999764, -2.183626157169999971, -143.0552959529999839 ) ) ;
#7522=VECTOR ( 'NONE', #19177, 1000.000000000000000 ) ;
#7542=DIRECTION ( 'NONE',  ( 0.000000000000000000, 1.000000000000000000, 0.000000000000000000 ) ) ;
#7558=CIRCLE ( 'NONE', #12881, 1.499999999999999556 ) ;
#7575=VECTOR ( 'NONE', #8229, 1000.000000000000000 ) ;
#7681=EDGE_LOOP ( 'NONE', ( #15615, #6372, #19248, #4281 ) ) ;
#7705=CARTESIAN_POINT ( 'NONE',  ( 3.249999999879999990, -3.000000000000000000, -135.4552959529999896 ) ) ;
#7801=ORIENTED_EDGE ( 'NONE', *, *, #6908, .F. ) ;
#7811=ORIENTED_EDGE ( 'NONE', *, *, #9768, .T. ) ;
#7813=VECTOR ( 'NONE', #21901, 1000.000000000000000 ) ;
#7852=FACE_OUTER_BOUND ( 'NONE', #10185, .T. ) ;
#7857=ADVANCED_FACE ( 'NONE', ( #21930 ), #12750, .T. ) ;
#7964=ADVANCED_FACE ( 'NONE', ( #7852 ), #739, .T. ) ;
#7974=CARTESIAN_POINT ( 'NONE',  ( 4.499999999879999102, -3.500000000000000000, -139.0552959529999839 ) ) ;
#8006=CARTESIAN_POINT ( 'NONE',  ( 3.999999999879999546, -3.500000000000000000, -135.4552959529999896 ) ) ;
#8064=ORIENTED_EDGE ( 'NONE', *, *, #4177, .F. ) ;
#8070=DIRECTION ( 'NONE',  ( 1.000000000000000000, 0.000000000000000000, 0.000000000000000000 ) ) ;
#8125=EDGE_CURVE ( 'NONE', #7013, #22055, #10227, .T. ) ;
#8229=DIRECTION ( 'NONE',  ( -1.000000000000000000, 0.000000000000000000, 0.000000000000000000 ) ) ;
#8280=CONICAL_SURFACE ( 'NONE', #9787, 1.499999999999999334, 0.9827937232469998730 ) ;
#8281=LINE ( 'NONE', #11730, #3786 ) ;
#8299=ORIENTED_EDGE ( 'NONE', *, *, #810, .F. ) ;
#8337=CARTESIAN_POINT ( 'NONE',  ( 4.499999999879999102, -4.000000000000000000, -132.3031539049999878 ) ) ;
#8394=VERTEX_POINT ( 'NONE', #942 ) ;
#8448=DIRECTION ( 'NONE',  ( -1.000000000000000000, 0.000000000000000000, 0.000000000000000000 ) ) ;
#8458=DIRECTION ( 'NONE',  ( -0.000000000000000000, 1.000000000000000000, 0.000000000000000000 ) ) ;
#8463=ORIENTED_EDGE ( 'NONE', *, *, #5488, .T. ) ;
#8483=DIRECTION ( 'NONE',  ( 0.000000000000000000, 0.000000000000000000, -1.000000000000000000 ) ) ;
#8505=VERTEX_POINT ( 'NONE', #5089 ) ;
#8530=CARTESIAN_POINT ( 'NONE',  ( 3.999999999879999546, -4.000000000000000000, -135.0552959530000123 ) ) ;
#8566=CARTESIAN_POINT ( 'NONE',  ( 4.499999999879999102, -1.500000000000000000, -135.4552959529999896 ) ) ;
#8593=LINE ( 'NONE', #11935, #21690 ) ;
#8614=VECTOR ( 'NONE', #11449, 1000.000000000000000 ) ;
#8633=MECHANICAL_DESIGN_GEOMETRIC_PRESENTATION_REPRESENTATION('',(#18914),#5239);
#8663=DIRECTION ( 'NONE',  ( 0.000000000000000000, -1.000000000000000000, 0.000000000000000000 ) ) ;
#8701=( NAMED_UNIT ( * ) PLANE_ANGLE_UNIT ( ) SI_UNIT ( $, .RADIAN. ) );
#8745=AXIS2_PLACEMENT_3D ( 'NONE', #1092, #17263, #17620 ) ;
#8768=EDGE_CURVE ( 'NONE', #21209, #8505, #10978, .T. ) ;
#8790=LINE ( 'NONE', #9143, #15221 ) ;
#8904=SURFACE_STYLE_FILL_AREA ( #21668 ) ;
#8930=AXIS2_PLACEMENT_3D ( 'NONE', #9307, #16581, #16471 ) ;
#8933=CIRCLE ( 'NONE', #994, 3.000000000000000000 ) ;
#8941=SHAPE_REPRESENTATION_RELATIONSHIP ( 'NONE' , 'NONE' ,  #15879, #3845 ) ;
#8961=LINE ( 'NONE', #1855, #23437 ) ;
#8977=CARTESIAN_POINT ( 'NONE',  ( 4.999999999879999990, -1.500000000000000000, -135.2552959529999725 ) ) ;
#9033=ORIENTED_EDGE ( 'NONE', *, *, #23005, .T. ) ;
#9099=ADVANCED_FACE ( 'NONE', ( #16504 ), #9456, .F. ) ;
#9143=CARTESIAN_POINT ( 'NONE',  ( 3.421292538029999886, -5.474560764249999600, -135.5552959530000123 ) ) ;
#9168=ORIENTED_EDGE ( 'NONE', *, *, #6255, .T. ) ;
#9222=( GEOMETRIC_REPRESENTATION_CONTEXT ( 3 ) GLOBAL_UNCERTAINTY_ASSIGNED_CONTEXT ( ( #21137 ) ) GLOBAL_UNIT_ASSIGNED_CONTEXT ( ( #15748, #8701, #3366 ) ) REPRESENTATION_CONTEXT ( 'NONE', 'WORKASPACE' ) );
#9307=CARTESIAN_POINT ( 'NONE',  ( 4.499999999879999102, -3.000000000000000000, -135.4552959529999896 ) ) ;
#9314=LINE ( 'NONE', #18276, #17165 ) ;
#9381=ORIENTED_EDGE ( 'NONE', *, *, #23005, .F. ) ;
#9384=EDGE_CURVE ( 'NONE', #23125, #1659, #7558, .T. ) ;
#9424=CARTESIAN_POINT ( 'NONE',  ( 5.749999999879999102, -4.000000000000000000, -135.0552959530000123 ) ) ;
#9456=PLANE ( 'NONE',  #21293 ) ;
#9460=ORIENTED_EDGE ( 'NONE', *, *, #9384, .F. ) ;
#9564=DIRECTION ( 'NONE',  ( -1.000000000000000000, 0.000000000000000000, 0.000000000000000000 ) ) ;
#9697=CARTESIAN_POINT ( 'NONE',  ( 4.999999999879999990, -4.000000000000000000, -135.4552959529999896 ) ) ;
#9742=ORIENTED_EDGE ( 'NONE', *, *, #11668, .F. ) ;
#9768=EDGE_CURVE ( 'NONE', #17827, #6145, #22599, .T. ) ;
#9771=DIRECTION ( 'NONE',  ( 0.000000000000000000, 0.000000000000000000, -1.000000000000000000 ) ) ;
#9787=AXIS2_PLACEMENT_3D ( 'NONE', #2926, #2808, #1159 ) ;
#9827=CARTESIAN_POINT ( 'NONE',  ( 3.999999999879999546, -3.000000000000000000, -135.0552959530000123 ) ) ;
#9837=DIRECTION ( 'NONE',  ( 0.000000000000000000, 0.000000000000000000, -1.000000000000000000 ) ) ;
#9986=FACE_OUTER_BOUND ( 'NONE', #6959, .T. ) ;
#9990=ORIENTED_EDGE ( 'NONE', *, *, #254, .F. ) ;
#10185=EDGE_LOOP ( 'NONE', ( #9460, #4095, #9168, #16218 ) ) ;
#10227=LINE ( 'NONE', #17498, #14442 ) ;
#10247=DIRECTION ( 'NONE',  ( -1.000000000000000000, 0.000000000000000000, 0.000000000000000000 ) ) ;
#10293=CARTESIAN_POINT ( 'NONE',  ( 5.749999999879999102, -3.000000000000000000, -135.4552959529999896 ) ) ;
#10324=ORIENTED_EDGE ( 'NONE', *, *, #19122, .F. ) ;
#10361=EDGE_CURVE ( 'NONE', #6401, #21499, #19942, .T. ) ;
#10392=DIRECTION ( 'NONE',  ( 1.000000000000000000, 0.000000000000000000, 0.000000000000000000 ) ) ;
#10418=DIRECTION ( 'NONE',  ( 1.000000000000000000, 0.000000000000000000, 0.000000000000000000 ) ) ;
#10449=LINE ( 'NONE', #4765, #16940 ) ;
#10476=CARTESIAN_POINT ( 'NONE',  ( 4.999999999879999990, -5.500000000000000000, -135.4552959529999896 ) ) ;
#10509=ADVANCED_FACE ( 'NONE', ( #11339 ), #4340, .T. ) ;
#10692=DIRECTION ( 'NONE',  ( 0.000000000000000000, 0.000000000000000000, 1.000000000000000000 ) ) ;
#10698=AXIS2_PLACEMENT_3D ( 'NONE', #21115, #8483, #13962 ) ;
#10726=( NAMED_UNIT ( * ) SI_UNIT ( $, .STERADIAN. ) SOLID_ANGLE_UNIT ( ) );
#10800=( NAMED_UNIT ( * ) PLANE_ANGLE_UNIT ( ) SI_UNIT ( $, .RADIAN. ) );
#10840=PRESENTATION_STYLE_ASSIGNMENT (( #16220 ) ) ;
#10841=ADVANCED_FACE ( 'NONE', ( #18938 ), #2772, .T. ) ;
#10860=DIRECTION ( 'NONE',  ( 0.000000000000000000, -1.000000000000000000, 0.000000000000000000 ) ) ;
#10926=CARTESIAN_POINT ( 'NONE',  ( 4.999999999879999990, -2.250000000000000000, -135.4552959529999896 ) ) ;
#10978=LINE ( 'NONE', #12885, #1927 ) ;
#10997=CARTESIAN_POINT ( 'NONE',  ( 3.999999999879999546, -1.500000000000000000, -135.0552959530000123 ) ) ;
#11011=AXIS2_PLACEMENT_3D ( 'NONE', #2338, #9564, #5650 ) ;
#11339=FACE_OUTER_BOUND ( 'NONE', #2480, .T. ) ;
#11449=DIRECTION ( 'NONE',  ( 0.000000000000000000, 0.000000000000000000, 1.000000000000000000 ) ) ;
#11473=VERTEX_POINT ( 'NONE', #3732 ) ;
#11571=PLANE ( 'NONE',  #4344 ) ;
#11650=DIRECTION ( 'NONE',  ( 0.4794255386042040601, 0.8775825618903723147, 0.000000000000000000 ) ) ;
#11668=EDGE_CURVE ( 'NONE', #13199, #4045, #22635, .T. ) ;
#11687=AXIS2_PLACEMENT_3D ( 'NONE', #7974, #22510, #11650 ) ;
#11730=CARTESIAN_POINT ( 'NONE',  ( 4.999999999879999990, -4.750000000000000000, -135.0552959530000123 ) ) ;
#11783=AXIS2_PLACEMENT_3D ( 'NONE', #7017, #10692, #21548 ) ;
#11789=ORIENTED_EDGE ( 'NONE', *, *, #17554, .F. ) ;
#11935=CARTESIAN_POINT ( 'NONE',  ( 2.499999999879999990, -4.000000000000000000, -135.2552959529999725 ) ) ;
#12018=DIRECTION ( 'NONE',  ( 0.000000000000000000, 1.000000000000000000, 0.000000000000000000 ) ) ;
#12029=LINE ( 'NONE', #8566, #7522 ) ;
#12069=PRODUCT_DEFINITION_CONTEXT ( 'detailed design', #7051, 'design' ) ;
#12115=VECTOR ( 'NONE', #8070, 1000.000000000000000 ) ;
#12136=EDGE_CURVE ( 'NONE', #1659, #11473, #21436, .T. ) ;
#12152=VECTOR ( 'NONE', #12587, 1000.000000000000000 ) ;
#12246=SURFACE_STYLE_USAGE ( .BOTH. , #5113 ) ;
#12298=EDGE_CURVE ( 'NONE', #6401, #21209, #4832, .T. ) ;
#12329=VERTEX_POINT ( 'NONE', #10997 ) ;
#12362=DIRECTION ( 'NONE',  ( 0.000000000000000000, 0.000000000000000000, 1.000000000000000000 ) ) ;
#12367=DIRECTION ( 'NONE',  ( -1.000000000000000000, 0.000000000000000000, 0.000000000000000000 ) ) ;
#12393=EDGE_CURVE ( 'NONE', #20527, #7013, #9314, .T. ) ;
#12442=ORIENTED_EDGE ( 'NONE', *, *, #6044, .F. ) ;
#12484=VECTOR ( 'NONE', #20114, 1000.000000000000000 ) ;
#12576=ORIENTED_EDGE ( 'NONE', *, *, #6041, .F. ) ;
#12587=DIRECTION ( 'NONE',  ( 0.000000000000000000, 0.000000000000000000, 1.000000000000000000 ) ) ;
#12640=FILL_AREA_STYLE ('',( #3609 ) ) ;
#12694=ORIENTED_EDGE ( 'NONE', *, *, #3709, .F. ) ;
#12750=PLANE ( 'NONE',  #1075 ) ;
#12784=DIRECTION ( 'NONE',  ( 0.000000000000000000, 0.000000000000000000, -1.000000000000000000 ) ) ;
#12793=ORIENTED_EDGE ( 'NONE', *, *, #1834, .F. ) ;
#12881=AXIS2_PLACEMENT_3D ( 'NONE', #13456, #20722, #4416 ) ;
#12885=CARTESIAN_POINT ( 'NONE',  ( 4.999999999879999990, -3.000000000000000000, -135.2552959529999725 ) ) ;
#12932=CONICAL_SURFACE ( 'NONE', #11783, 1.499999999999999334, 0.9827937232469998730 ) ;
#12970=VECTOR ( 'NONE', #14585, 1000.000000000000000 ) ;
#13042=ORIENTED_EDGE ( 'NONE', *, *, #21584, .F. ) ;
#13046=ORIENTED_EDGE ( 'NONE', *, *, #3709, .T. ) ;
#13072=CARTESIAN_POINT ( 'NONE',  ( 2.499999999879999990, -3.000000000000000000, -135.0552959530000123 ) ) ;
#13127=APPLICATION_CONTEXT ( 'automotive_design' ) ;
#13199=VERTEX_POINT ( 'NONE', #15453 ) ;
#13277=CIRCLE ( 'NONE', #3045, 1.499999999999999556 ) ;
#13330=CARTESIAN_POINT ( 'NONE',  ( 3.999999999879999546, -3.000000000000000000, -135.4552959529999896 ) ) ;
#13429=CARTESIAN_POINT ( 'NONE',  ( 3.249999999879999990, -3.000000000000000000, -135.0552959530000123 ) ) ;
#13456=CARTESIAN_POINT ( 'NONE',  ( 4.499999999879999102, -3.500000000000000000, -143.0552959529999839 ) ) ;
#13490=ORIENTED_EDGE ( 'NONE', *, *, #21142, .F. ) ;
#13548=ADVANCED_FACE ( 'NONE', ( #13879 ), #20914, .T. ) ;
#13598=ORIENTED_EDGE ( 'NONE', *, *, #1834, .T. ) ;
#13694=CARTESIAN_POINT ( 'NONE',  ( 3.999999999879999546, -2.250000000000000000, -135.0552959530000123 ) ) ;
#13838=CARTESIAN_POINT ( 'NONE',  ( 3.249999999879999990, -4.000000000000000000, -135.0552959530000123 ) ) ;
#13879=FACE_OUTER_BOUND ( 'NONE', #2746, .T. ) ;
#13903=ORIENTED_EDGE ( 'NONE', *, *, #20716, .T. ) ;
#13913=DIRECTION ( 'NONE',  ( 0.000000000000000000, 0.000000000000000000, -1.000000000000000000 ) ) ;
#13962=DIRECTION ( 'NONE',  ( 1.000000000000000000, 0.000000000000000000, 0.000000000000000000 ) ) ;
#14001=VECTOR ( 'NONE', #17623, 1000.000000000000000 ) ;
#14017=ORIENTED_EDGE ( 'NONE', *, *, #20716, .F. ) ;
#14034=VECTOR ( 'NONE', #4728, 1000.000000000000000 ) ;
#14069=LINE ( 'NONE', #3014, #6420 ) ;
#14170=FACE_OUTER_BOUND ( 'NONE', #22371, .T. ) ;
#14220=PLANE ( 'NONE',  #15075 ) ;
#14264=CARTESIAN_POINT ( 'NONE',  ( 4.999999999879999990, -4.000000000000000000, -135.2552959529999725 ) ) ;
#14442=VECTOR ( 'NONE', #8448, 1000.000000000000000 ) ;
#14448=PRODUCT_DEFINITION ( 'UNKNOWN', '', #3943, #12069 ) ;
#14475=DIRECTION ( 'NONE',  ( 0.000000000000000000, 0.000000000000000000, -1.000000000000000000 ) ) ;
#14523=EDGE_LOOP ( 'NONE', ( #5672, #6606, #15922, #5787 ) ) ;
#14529=CARTESIAN_POINT ( 'NONE',  ( 3.999999999879999546, -2.250000000000000000, -135.4552959529999896 ) ) ;
#14532=AXIS2_PLACEMENT_3D ( 'NONE', #1256, #17296, #19196 ) ;
#14559=( NAMED_UNIT ( * ) PLANE_ANGLE_UNIT ( ) SI_UNIT ( $, .RADIAN. ) );
#14576=DIRECTION ( 'NONE',  ( -0.000000000000000000, 1.000000000000000000, 0.000000000000000000 ) ) ;
#14578=PLANE ( 'NONE',  #8930 ) ;
#14585=DIRECTION ( 'NONE',  ( 0.000000000000000000, 1.000000000000000000, 0.000000000000000000 ) ) ;
#14605=EDGE_LOOP ( 'NONE', ( #22474, #297 ) ) ;
#14613=ORIENTED_EDGE ( 'NONE', *, *, #6255, .F. ) ;
#14633=CARTESIAN_POINT ( 'NONE',  ( 6.499999999879999102, -3.500000000000000000, -135.0552959530000123 ) ) ;
#14652=ORIENTED_EDGE ( 'NONE', *, *, #1406, .T. ) ;
#14672=EDGE_CURVE ( 'NONE', #22590, #4093, #2329, .T. ) ;
#14711=ORIENTED_EDGE ( 'NONE', *, *, #11668, .T. ) ;
#14717=DIRECTION ( 'NONE',  ( -0.000000000000000000, 1.000000000000000000, 0.000000000000000000 ) ) ;
#14778=DIRECTION ( 'NONE',  ( 1.000000000000000000, 0.000000000000000000, 0.000000000000000000 ) ) ;
#14788=DIRECTION ( 'NONE',  ( 0.000000000000000000, 0.000000000000000000, 1.000000000000000000 ) ) ;
#14867=ORIENTED_EDGE ( 'NONE', *, *, #10361, .F. ) ;
#14971=CARTESIAN_POINT ( 'NONE',  ( 4.499999999879999102, -3.500000000000000000, -136.0552959530000123 ) ) ;
#15027=FACE_OUTER_BOUND ( 'NONE', #14605, .T. ) ;
#15031=CARTESIAN_POINT ( 'NONE',  ( 3.999999999879999546, -4.750000000000000000, -135.0552959530000123 ) ) ;
#15075=AXIS2_PLACEMENT_3D ( 'NONE', #18265, #14576, #16124 ) ;
#15221=VECTOR ( 'NONE', #16423, 1000.000000000000000 ) ;
#15265=EDGE_LOOP ( 'NONE', ( #14017, #4110, #20287, #841 ) ) ;
#15272=CARTESIAN_POINT ( 'NONE',  ( 6.499999999879999102, -4.000000000000000000, -135.4552959529999896 ) ) ;
#15278=CARTESIAN_POINT ( 'NONE',  ( 5.749999999879999102, -4.000000000000000000, -135.4552959529999896 ) ) ;
#15290=DIRECTION ( 'NONE',  ( 1.000000000000000000, 0.000000000000000000, 0.000000000000000000 ) ) ;
#15325=CARTESIAN_POINT ( 'NONE',  ( 3.999999999879999546, -4.000000000000000000, -135.2552959529999725 ) ) ;
#15326=VERTEX_POINT ( 'NONE', #4235 ) ;
#15338=CARTESIAN_POINT ( 'NONE',  ( 6.499999999879999102, -4.000000000000000000, -135.2552959529999725 ) ) ;
#15453=CARTESIAN_POINT ( 'NONE',  ( 3.999999999879999546, -4.000000000000000000, -135.4552959529999896 ) ) ;
#15460=CARTESIAN_POINT ( 'NONE',  ( 4.499999999879999102, -3.500000000000000000, -139.0552959529999839 ) ) ;
#15487=EDGE_CURVE ( 'NONE', #21810, #1162, #8933, .T. ) ;
#15597=DIRECTION ( 'NONE',  ( -1.000000000000000000, 0.000000000000000000, 0.000000000000000000 ) ) ;
#15612=DIRECTION ( 'NONE',  ( 1.000000000000000000, 0.000000000000000000, 0.000000000000000000 ) ) ;
#15615=ORIENTED_EDGE ( 'NONE', *, *, #12298, .F. ) ;
#15626=DIRECTION ( 'NONE',  ( 0.000000000000000000, 0.000000000000000000, -1.000000000000000000 ) ) ;
#15653=CARTESIAN_POINT ( 'NONE',  ( 4.499999999879999102, -3.500000000000000000, -135.0552959530000123 ) ) ;
#15675=CARTESIAN_POINT ( 'NONE',  ( 2.499999999879999990, -3.500000000000000000, -143.0552959529999839 ) ) ;
#15748=( LENGTH_UNIT ( ) NAMED_UNIT ( * ) SI_UNIT ( .MILLI., .METRE. ) );
#15826=PLANE ( 'NONE',  #8745 ) ;
#15829=CARTESIAN_POINT ( 'NONE',  ( 2.499999999879999990, -3.500000000000000000, -135.0552959530000123 ) ) ;
#15877=ADVANCED_FACE ( 'NONE', ( #15027 ), #17285, .T. ) ;
#15879=SHAPE_REPRESENTATION ( 'Phillips Screw', ( #5025 ), #9222 ) ;
#15906=ORIENTED_EDGE ( 'NONE', *, *, #8125, .T. ) ;
#15921=AXIS2_PLACEMENT_3D ( 'NONE', #15460, #13913, #17362 ) ;
#15922=ORIENTED_EDGE ( 'NONE', *, *, #2753, .T. ) ;
#16124=DIRECTION ( 'NONE',  ( 1.000000000000000000, 0.000000000000000000, 0.000000000000000000 ) ) ;
#16146=ORIENTED_EDGE ( 'NONE', *, *, #18960, .T. ) ;
#16178=ORIENTED_EDGE ( 'NONE', *, *, #12136, .T. ) ;
#16193=CARTESIAN_POINT ( 'NONE',  ( 3.780861691979999772, -4.816373842840000030, -139.5552959529999839 ) ) ;
#16211=LINE ( 'NONE', #21454, #1039 ) ;
#16218=ORIENTED_EDGE ( 'NONE', *, *, #12136, .F. ) ;
#16220=SURFACE_STYLE_USAGE ( .BOTH. , #713 ) ;
#16256=VERTEX_POINT ( 'NONE', #13330 ) ;
#16258=CARTESIAN_POINT ( 'NONE',  ( 5.938276615700000427, -0.8672523143300000514, -135.0552959530000123 ) ) ;
#16264=ORIENTED_EDGE ( 'NONE', *, *, #18400, .T. ) ;
#16411=VECTOR ( 'NONE', #17977, 1000.000000000000000 ) ;
#16423=DIRECTION ( 'NONE',  ( -0.3989061605089001539, -0.7301928289268172501, 0.5547001962248612195 ) ) ;
#16458=COLOUR_RGB ( '', 0.40784314, 0.44705882, 0.49803922) ;
#16471=DIRECTION ( 'NONE',  ( 0.000000000000000000, 0.000000000000000000, -1.000000000000000000 ) ) ;
#16504=FACE_OUTER_BOUND ( 'NONE', #17241, .T. ) ;
#16581=DIRECTION ( 'NONE',  ( 0.000000000000000000, -1.000000000000000000, 0.000000000000000000 ) ) ;
#16600=AXIS2_PLACEMENT_3D ( 'NONE', #14971, #18320, #7367 ) ;
#16612=CARTESIAN_POINT ( 'NONE',  ( 5.219138307789999764, -2.183626157169999971, -139.5552959529999839 ) ) ;
#16785=ORIENTED_EDGE ( 'NONE', *, *, #6740, .T. ) ;
#16822=CARTESIAN_POINT ( 'NONE',  ( 4.499999999879999102, -3.000000000000000000, -135.4552959529999896 ) ) ;
#16826=ORIENTED_EDGE ( 'NONE', *, *, #16953, .F. ) ;
#16848=CARTESIAN_POINT ( 'NONE',  ( 4.999999999879999990, -4.000000000000000000, -135.0552959530000123 ) ) ;
#16871=ADVANCED_FACE ( 'NONE', ( #2088 ), #14578, .T. ) ;
#16874=VECTOR ( 'NONE', #14788, 1000.000000000000000 ) ;
#16940=VECTOR ( 'NONE', #8663, 1000.000000000000000 ) ;
#16953=EDGE_CURVE ( 'NONE', #4267, #21050, #17173, .T. ) ;
#16958=CARTESIAN_POINT ( 'NONE',  ( 6.499999999879999102, -3.000000000000000000, -135.4552959529999896 ) ) ;
#17084=DIRECTION ( 'NONE',  ( 0.000000000000000000, 0.000000000000000000, 1.000000000000000000 ) ) ;
#17165=VECTOR ( 'NONE', #12784, 1000.000000000000000 ) ;
#17170=CARTESIAN_POINT ( 'NONE',  ( 6.499999999879999102, -3.000000000000000000, -135.0552959530000123 ) ) ;
#17171=PLANE ( 'NONE',  #661 ) ;
#17173=LINE ( 'NONE', #15031, #1367 ) ;
#17241=EDGE_LOOP ( 'NONE', ( #22284, #5418, #2036, #8064 ) ) ;
#17263=DIRECTION ( 'NONE',  ( -0.000000000000000000, 1.000000000000000000, 0.000000000000000000 ) ) ;
#17285=PLANE ( 'NONE',  #22655 ) ;
#17296=DIRECTION ( 'NONE',  ( 0.000000000000000000, 0.000000000000000000, -1.000000000000000000 ) ) ;
#17362=DIRECTION ( 'NONE',  ( 0.4794255386042040601, 0.8775825618903723147, 0.000000000000000000 ) ) ;
#17446=CARTESIAN_POINT ( 'NONE',  ( 6.499999999879999102, -4.000000000000000000, -135.0552959530000123 ) ) ;
#17485=CYLINDRICAL_SURFACE ( 'NONE', #15921, 1.499999999999999334 ) ;
#17498=CARTESIAN_POINT ( 'NONE',  ( 4.499999999879999102, -5.500000000000000000, -135.4552959529999896 ) ) ;
#17515=EDGE_CURVE ( 'NONE', #1015, #7013, #10449, .T. ) ;
#17526=FACE_OUTER_BOUND ( 'NONE', #20584, .T. ) ;
#17554=EDGE_CURVE ( 'NONE', #4093, #21499, #5228, .T. ) ;
#17571=DIRECTION ( 'NONE',  ( -1.000000000000000000, 0.000000000000000000, 0.000000000000000000 ) ) ;
#17617=FACE_OUTER_BOUND ( 'NONE', #681, .T. ) ;
#17620=DIRECTION ( 'NONE',  ( 1.000000000000000000, 0.000000000000000000, 0.000000000000000000 ) ) ;
#17623=DIRECTION ( 'NONE',  ( 0.000000000000000000, 1.000000000000000000, 0.000000000000000000 ) ) ;
#17624=EDGE_LOOP ( 'NONE', ( #9990, #16178, #16146, #13490 ) ) ;
#17628=DIRECTION ( 'NONE',  ( 0.000000000000000000, 1.000000000000000000, 0.000000000000000000 ) ) ;
#17645=CARTESIAN_POINT ( 'NONE',  ( 4.499999999879999102, -3.500000000000000000, -135.0552959530000123 ) ) ;
#17827=VERTEX_POINT ( 'NONE', #13072 ) ;
#17831=VECTOR ( 'NONE', #6020, 1000.000000000000000 ) ;
#17977=DIRECTION ( 'NONE',  ( 0.000000000000000000, -1.000000000000000000, 0.000000000000000000 ) ) ;
#18007=( LENGTH_UNIT ( ) NAMED_UNIT ( * ) SI_UNIT ( .MILLI., .METRE. ) );
#18014=ORIENTED_EDGE ( 'NONE', *, *, #12298, .T. ) ;
#18085=( NAMED_UNIT ( * ) SI_UNIT ( $, .STERADIAN. ) SOLID_ANGLE_UNIT ( ) );
#18241=CARTESIAN_POINT ( 'NONE',  ( 3.999999999879999546, -3.500000000000000000, -135.4552959529999896 ) ) ;
#18265=CARTESIAN_POINT ( 'NONE',  ( 4.499999999879999102, -5.500000000000000000, -143.0552959529999839 ) ) ;
#18276=CARTESIAN_POINT ( 'NONE',  ( 4.999999999879999990, -5.500000000000000000, -135.2552959529999725 ) ) ;
#18304=PRODUCT_CONTEXT ( 'NONE', #13127, 'mechanical' ) ;
#18320=DIRECTION ( 'NONE',  ( 0.000000000000000000, 0.000000000000000000, -1.000000000000000000 ) ) ;
#18400=EDGE_CURVE ( 'NONE', #3916, #1162, #20735, .T. ) ;
#18427=LINE ( 'NONE', #7705, #18503 ) ;
#18495=EDGE_LOOP ( 'NONE', ( #4542, #6727, #9742, #18774, #1191, #884, #13042, #7466, #18014, #9381, #2911, #13903 ) ) ;
#18503=VECTOR ( 'NONE', #468, 1000.000000000000000 ) ;
#18642=ORIENTED_EDGE ( 'NONE', *, *, #15487, .F. ) ;
#18689=VECTOR ( 'NONE', #17571, 1000.000000000000000 ) ;
#18729=DIRECTION ( 'NONE',  ( 0.000000000000000000, 0.000000000000000000, -1.000000000000000000 ) ) ;
#18774=ORIENTED_EDGE ( 'NONE', *, *, #19122, .T. ) ;
#18896=PLANE ( 'NONE',  #462 ) ;
#18914=STYLED_ITEM ( 'NONE', ( #3218 ), #19750 ) ;
#18935=LINE ( 'NONE', #3790, #19470 ) ;
#18938=FACE_OUTER_BOUND ( 'NONE', #6448, .T. ) ;
#18951=EDGE_CURVE ( 'NONE', #16256, #3279, #18427, .T. ) ;
#18960=EDGE_CURVE ( 'NONE', #11473, #3916, #23068, .T. ) ;
#18994=ORIENTED_EDGE ( 'NONE', *, *, #1940, .F. ) ;
#19002=DIRECTION ( 'NONE',  ( 0.000000000000000000, 1.000000000000000000, 0.000000000000000000 ) ) ;
#19050=LINE ( 'NONE', #13694, #14001 ) ;
#19054=VECTOR ( 'NONE', #23446, 1000.000000000000000 ) ;
#19078=DIRECTION ( 'NONE',  ( 0.000000000000000000, 1.000000000000000000, 0.000000000000000000 ) ) ;
#19097=ADVANCED_FACE ( 'NONE', ( #21726 ), #14220, .T. ) ;
#19101=AXIS2_PLACEMENT_3D ( 'NONE', #15675, #926, #19002 ) ;
#19122=EDGE_CURVE ( 'NONE', #13199, #22055, #8961, .T. ) ;
#19177=DIRECTION ( 'NONE',  ( -1.000000000000000000, 0.000000000000000000, 0.000000000000000000 ) ) ;
#19186=DIRECTION ( 'NONE',  ( 1.000000000000000000, 0.000000000000000000, 0.000000000000000000 ) ) ;
#19196=DIRECTION ( 'NONE',  ( 1.000000000000000000, 0.000000000000000000, 0.000000000000000000 ) ) ;
#19248=ORIENTED_EDGE ( 'NONE', *, *, #5864, .F. ) ;
#19326=VECTOR ( 'NONE', #12018, 1000.000000000000000 ) ;
#19346=ADVANCED_FACE ( 'NONE', ( #2199 ), #22413, .T. ) ;
#19370=DIRECTION ( 'NONE',  ( 0.000000000000000000, 1.000000000000000000, 0.000000000000000000 ) ) ;
#19401=ADVANCED_FACE ( 'NONE', ( #20866, #17526 ), #17171, .F. ) ;
#19406=DIRECTION ( 'NONE',  ( 0.000000000000000000, 0.000000000000000000, 1.000000000000000000 ) ) ;
#19470=VECTOR ( 'NONE', #17628, 1000.000000000000000 ) ;
#19529=LINE ( 'NONE', #15829, #19326 ) ;
#19594=ADVANCED_FACE ( 'NONE', ( #17617 ), #6776, .T. ) ;
#19709=LINE ( 'NONE', #8977, #2705 ) ;
#19749=ORIENTED_EDGE ( 'NONE', *, *, #16953, .T. ) ;
#19750=MANIFOLD_SOLID_BREP ( 'lock_assembly.1\\Part1.2\\PartBody', #6887 ) ;
#19881=FACE_OUTER_BOUND ( 'NONE', #5821, .T. ) ;
#19911=SURFACE_STYLE_FILL_AREA ( #12640 ) ;
#19942=LINE ( 'NONE', #83, #6063 ) ;
#19987=( LENGTH_UNIT ( ) NAMED_UNIT ( * ) SI_UNIT ( .MILLI., .METRE. ) );
#20011=ORIENTED_EDGE ( 'NONE', *, *, #6908, .T. ) ;
#20025=CARTESIAN_POINT ( 'NONE',  ( 4.999999999879999990, -5.500000000000000000, -135.0552959530000123 ) ) ;
#20114=DIRECTION ( 'NONE',  ( 0.000000000000000000, -1.000000000000000000, 0.000000000000000000 ) ) ;
#20173=VECTOR ( 'NONE', #12367, 1000.000000000000000 ) ;
#20186=ORIENTED_EDGE ( 'NONE', *, *, #12393, .T. ) ;
#20231=ORIENTED_EDGE ( 'NONE', *, *, #6041, .T. ) ;
#20287=ORIENTED_EDGE ( 'NONE', *, *, #20662, .F. ) ;
#20291=ADVANCED_FACE ( 'NONE', ( #4588 ), #8280, .T. ) ;
#20420=ORIENTED_EDGE ( 'NONE', *, *, #1406, .F. ) ;
#20431=SHAPE_DEFINITION_REPRESENTATION ( #23266, #15879 ) ;
#20498=VECTOR ( 'NONE', #5056, 1000.000000000000000 ) ;
#20527=VERTEX_POINT ( 'NONE', #20025 ) ;
#20584=EDGE_LOOP ( 'NONE', ( #3598, #18642 ) ) ;
#20631=CARTESIAN_POINT ( 'NONE',  ( 4.499999999879999102, -2.000000000000000000, -143.0552959529999839 ) ) ;
#20659=EDGE_CURVE ( 'NONE', #3396, #17827, #19529, .T. ) ;
#20662=EDGE_CURVE ( 'NONE', #6145, #12329, #19050, .T. ) ;
#20702=ORIENTED_EDGE ( 'NONE', *, *, #17554, .T. ) ;
#20716=EDGE_CURVE ( 'NONE', #21412, #16256, #5363, .T. ) ;
#20722=DIRECTION ( 'NONE',  ( 0.000000000000000000, 0.000000000000000000, -1.000000000000000000 ) ) ;
#20735=LINE ( 'NONE', #5858, #5168 ) ;
#20769=ADVANCED_FACE ( 'NONE', ( #14170 ), #6902, .F. ) ;
#20797=EDGE_CURVE ( 'NONE', #22055, #4267, #5118, .T. ) ;
#20866=FACE_BOUND ( 'NONE', #1945, .T. ) ;
#20914=PLANE ( 'NONE',  #19101 ) ;
#20924=LINE ( 'NONE', #15325, #14034 ) ;
#21022=CARTESIAN_POINT ( 'NONE',  ( 4.999999999879999990, -3.000000000000000000, -135.4552959529999896 ) ) ;
#21036=EDGE_CURVE ( 'NONE', #4093, #5749, #6283, .T. ) ;
#21050=VERTEX_POINT ( 'NONE', #8530 ) ;
#21095=CARTESIAN_POINT ( 'NONE',  ( 3.249999999879999990, -4.000000000000000000, -135.4552959529999896 ) ) ;
#21115=CARTESIAN_POINT ( 'NONE',  ( 4.499999999879999102, -3.500000000000000000, -135.0552959530000123 ) ) ;
#21117=ORIENTED_EDGE ( 'NONE', *, *, #20659, .F. ) ;
#21137=UNCERTAINTY_MEASURE_WITH_UNIT (LENGTH_MEASURE( 1.000000000000000082E-05 ), #15748, 'distance_accuracy_value', 'NONE');
#21142=EDGE_CURVE ( 'NONE', #23125, #3916, #22326, .T. ) ;
#21169=DIRECTION ( 'NONE',  ( 0.000000000000000000, -1.000000000000000000, 0.000000000000000000 ) ) ;
#21209=VERTEX_POINT ( 'NONE', #21022 ) ;
#21293=AXIS2_PLACEMENT_3D ( 'NONE', #7454, #14717, #5673 ) ;
#21314=CARTESIAN_POINT ( 'NONE',  ( 3.780861691979999772, -4.816373842840000030, -143.0552959529999839 ) ) ;
#21335=DIRECTION ( 'NONE',  ( 1.000000000000000000, 0.000000000000000000, 0.000000000000000000 ) ) ;
#21336=ORIENTED_EDGE ( 'NONE', *, *, #6044, .T. ) ;
#21366=CARTESIAN_POINT ( 'NONE',  ( 2.499999999879999990, -3.000000000000000000, -135.2552959529999725 ) ) ;
#21385=LINE ( 'NONE', #3639, #12970 ) ;
#21396=DIRECTION ( 'NONE',  ( 0.000000000000000000, 0.000000000000000000, -1.000000000000000000 ) ) ;
#21412=VERTEX_POINT ( 'NONE', #1594 ) ;
#21436=LINE ( 'NONE', #16193, #19054 ) ;
#21454=CARTESIAN_POINT ( 'NONE',  ( 4.499999999879999102, -5.500000000000000000, -135.0552959530000123 ) ) ;
#21499=VERTEX_POINT ( 'NONE', #17170 ) ;
#21548=DIRECTION ( 'NONE',  ( 0.4794255386042040601, 0.8775825618903723147, 0.000000000000000000 ) ) ;
#21582=AXIS2_PLACEMENT_3D ( 'NONE', #16822, #6225, #9771 ) ;
#21584=EDGE_CURVE ( 'NONE', #5749, #1015, #4680, .T. ) ;
#21625=ORIENTED_EDGE ( 'NONE', *, *, #8768, .T. ) ;
#21668=FILL_AREA_STYLE ('',( #3573 ) ) ;
#21690=VECTOR ( 'NONE', #23133, 1000.000000000000000 ) ;
#21726=FACE_OUTER_BOUND ( 'NONE', #21729, .T. ) ;
#21729=EDGE_LOOP ( 'NONE', ( #20186, #15906, #1612, #7801 ) ) ;
#21794=LINE ( 'NONE', #10926, #16411 ) ;
#21810=VERTEX_POINT ( 'NONE', #7012 ) ;
#21901=DIRECTION ( 'NONE',  ( 0.000000000000000000, 1.000000000000000000, 0.000000000000000000 ) ) ;
#21915=CARTESIAN_POINT ( 'NONE',  ( 2.499999999879999990, -3.000000000000000000, -135.4552959529999896 ) ) ;
#21930=FACE_OUTER_BOUND ( 'NONE', #22596, .T. ) ;
#21991=CARTESIAN_POINT ( 'NONE',  ( 5.219138307789999764, -2.183626157169999971, -136.0552959530000123 ) ) ;
#22055=VERTEX_POINT ( 'NONE', #2833 ) ;
#22076=EDGE_LOOP ( 'NONE', ( #14613, #16264, #657, #12793 ) ) ;
#22178=DIRECTION ( 'NONE',  ( 0.000000000000000000, -1.000000000000000000, 0.000000000000000000 ) ) ;
#22284=ORIENTED_EDGE ( 'NONE', *, *, #1940, .T. ) ;
#22326=LINE ( 'NONE', #16612, #17831 ) ;
#22371=EDGE_LOOP ( 'NONE', ( #20702, #14867, #8299, #3771 ) ) ;
#22413=PLANE ( 'NONE',  #21582 ) ;
#22474=ORIENTED_EDGE ( 'NONE', *, *, #9384, .T. ) ;
#22510=DIRECTION ( 'NONE',  ( 0.000000000000000000, 0.000000000000000000, -1.000000000000000000 ) ) ;
#22590=VERTEX_POINT ( 'NONE', #16848 ) ;
#22596=EDGE_LOOP ( 'NONE', ( #16826, #22604, #10324, #20231 ) ) ;
#22599=LINE ( 'NONE', #13429, #12115 ) ;
#22604=ORIENTED_EDGE ( 'NONE', *, *, #20797, .F. ) ;
#22635=LINE ( 'NONE', #21095, #45 ) ;
#22655=AXIS2_PLACEMENT_3D ( 'NONE', #20631, #18729, #22178 ) ;
#22718=COLOUR_RGB ( '', 0.40784314, 0.44705882, 0.49803922) ;
#22761=LINE ( 'NONE', #13838, #4442 ) ;
#22799=UNCERTAINTY_MEASURE_WITH_UNIT (LENGTH_MEASURE( 1.000000000000000082E-05 ), #18007, 'distance_accuracy_value', 'NONE');
#22811=CARTESIAN_POINT ( 'NONE',  ( 2.499999999879999990, -4.000000000000000000, -135.4552959529999896 ) ) ;
#22884=CIRCLE ( 'NONE', #14532, 1.499999999999999556 ) ;
#22893=DIRECTION ( 'NONE',  ( 0.000000000000000000, -1.000000000000000000, 0.000000000000000000 ) ) ;
#22916=MECHANICAL_DESIGN_GEOMETRIC_PRESENTATION_REPRESENTATION('',(#4296),#4670);
#23005=EDGE_CURVE ( 'NONE', #8394, #21209, #21794, .T. ) ;
#23068=CIRCLE ( 'NONE', #16600, 1.499999999999999556 ) ;
#23125=VERTEX_POINT ( 'NONE', #7482 ) ;
#23133=DIRECTION ( 'NONE',  ( 0.000000000000000000, 0.000000000000000000, -1.000000000000000000 ) ) ;
#23139=LINE ( 'NONE', #21366, #20498 ) ;
#23212=CARTESIAN_POINT ( 'NONE',  ( 3.999999999879999546, -5.500000000000000000, -135.2552959529999725 ) ) ;
#23245=ADVANCED_FACE ( 'NONE', ( #943 ), #18896, .F. ) ;
#23266=PRODUCT_DEFINITION_SHAPE ( 'NONE', 'NONE',  #14448 ) ;
#23437=VECTOR ( 'NONE', #10860, 1000.000000000000000 ) ;
#23446=DIRECTION ( 'NONE',  ( 0.000000000000000000, 0.000000000000000000, 1.000000000000000000 ) ) ;
#23463=DIRECTION ( 'NONE',  ( -1.000000000000000000, 0.000000000000000000, 0.000000000000000000 ) ) ;
#23498=UNCERTAINTY_MEASURE_WITH_UNIT (LENGTH_MEASURE( 1.000000000000000082E-05 ), #19987, 'distance_accuracy_value', 'NONE');
ENDSEC;
END-ISO-10303-21;
